ISO-10303-21;
HEADER;
/* Generated by software containing ST-Developer
 * from STEP Tools, Inc. (www.steptools.com) 
 */

FILE_DESCRIPTION(
/* description */ ('Double-row support with tensioned shaft'),
/* implementation_level */ '2;1');

FILE_NAME(
/* name */ 'Hex Nut - M8.step',
/* time_stamp */ '2026-10-27T10:50:35-07:00',
/* author */ (''),
/* organization */ (''),
/* preprocessor_version */ 'ST-DEVELOPER v20.2',
/* originating_system */ 'Autodesk Translation Framework v15.17.0.0',
/* authorisation */ '');

FILE_SCHEMA (('AUTOMOTIVE_DESIGN { 1 0 10303 214 3 1 1 }'));
ENDSEC;

DATA;
#10=MECHANICAL_DESIGN_GEOMETRIC_PRESENTATION_REPRESENTATION('',(#503),#11559);
#11=(
BOUNDED_CURVE()
B_SPLINE_CURVE(2,(#10913,#10914,#10915),.UNSPECIFIED.,.F.,.F.)
B_SPLINE_CURVE_WITH_KNOTS((3,3),(0.14973948338295,0.97160236658079),
 .UNSPECIFIED.)
CURVE()
GEOMETRIC_REPRESENTATION_ITEM()
RATIONAL_B_SPLINE_CURVE((1.07140024848292,1.23714644374248,1.07140024848292))
REPRESENTATION_ITEM('')
);
#12=(
BOUNDED_CURVE()
B_SPLINE_CURVE(2,(#10917,#10918,#10919),.UNSPECIFIED.,.F.,.F.)
B_SPLINE_CURVE_WITH_KNOTS((3,3),(0.14973948338295,0.971602366580789),
 .UNSPECIFIED.)
CURVE()
GEOMETRIC_REPRESENTATION_ITEM()
RATIONAL_B_SPLINE_CURVE((1.07140024848292,1.23714644374248,1.07140024848292))
REPRESENTATION_ITEM('')
);
#13=(
BOUNDED_CURVE()
B_SPLINE_CURVE(2,(#10924,#10925,#10926),.UNSPECIFIED.,.F.,.F.)
B_SPLINE_CURVE_WITH_KNOTS((3,3),(0.14973948338295,0.97160236658079),
 .UNSPECIFIED.)
CURVE()
GEOMETRIC_REPRESENTATION_ITEM()
RATIONAL_B_SPLINE_CURVE((1.07140024848292,1.23714644374248,1.07140024848292))
REPRESENTATION_ITEM('')
);
#14=(
BOUNDED_CURVE()
B_SPLINE_CURVE(2,(#10928,#10929,#10930),.UNSPECIFIED.,.F.,.F.)
B_SPLINE_CURVE_WITH_KNOTS((3,3),(0.14973948338295,0.97160236658079),
 .UNSPECIFIED.)
CURVE()
GEOMETRIC_REPRESENTATION_ITEM()
RATIONAL_B_SPLINE_CURVE((1.07140024848292,1.23714644374248,1.07140024848292))
REPRESENTATION_ITEM('')
);
#15=(
BOUNDED_CURVE()
B_SPLINE_CURVE(2,(#10932,#10933,#10934),.UNSPECIFIED.,.F.,.F.)
B_SPLINE_CURVE_WITH_KNOTS((3,3),(0.14973948338295,0.971602366580789),
 .UNSPECIFIED.)
CURVE()
GEOMETRIC_REPRESENTATION_ITEM()
RATIONAL_B_SPLINE_CURVE((1.07140024848292,1.23714644374248,1.07140024848292))
REPRESENTATION_ITEM('')
);
#16=(
BOUNDED_CURVE()
B_SPLINE_CURVE(2,(#10935,#10936,#10937),.UNSPECIFIED.,.F.,.F.)
B_SPLINE_CURVE_WITH_KNOTS((3,3),(0.14973948338295,0.97160236658079),
 .UNSPECIFIED.)
CURVE()
GEOMETRIC_REPRESENTATION_ITEM()
RATIONAL_B_SPLINE_CURVE((1.07140024848292,1.23714644374248,1.07140024848292))
REPRESENTATION_ITEM('')
);
#17=(
BOUNDED_CURVE()
B_SPLINE_CURVE(2,(#10944,#10945,#10946),.UNSPECIFIED.,.F.,.F.)
B_SPLINE_CURVE_WITH_KNOTS((3,3),(0.14973948338295,0.97160236658079),
 .UNSPECIFIED.)
CURVE()
GEOMETRIC_REPRESENTATION_ITEM()
RATIONAL_B_SPLINE_CURVE((1.07140024848292,1.23714644374248,1.07140024848292))
REPRESENTATION_ITEM('')
);
#18=(
BOUNDED_CURVE()
B_SPLINE_CURVE(2,(#10948,#10949,#10950),.UNSPECIFIED.,.F.,.F.)
B_SPLINE_CURVE_WITH_KNOTS((3,3),(0.14973948338295,0.97160236658079),
 .UNSPECIFIED.)
CURVE()
GEOMETRIC_REPRESENTATION_ITEM()
RATIONAL_B_SPLINE_CURVE((1.07140024848292,1.23714644374248,1.07140024848292))
REPRESENTATION_ITEM('')
);
#19=(
BOUNDED_CURVE()
B_SPLINE_CURVE(2,(#10952,#10953,#10954),.UNSPECIFIED.,.F.,.F.)
B_SPLINE_CURVE_WITH_KNOTS((3,3),(0.14973948338295,0.971602366580789),
 .UNSPECIFIED.)
CURVE()
GEOMETRIC_REPRESENTATION_ITEM()
RATIONAL_B_SPLINE_CURVE((1.07140024848292,1.23714644374248,1.07140024848292))
REPRESENTATION_ITEM('')
);
#20=(
BOUNDED_CURVE()
B_SPLINE_CURVE(2,(#10956,#10957,#10958),.UNSPECIFIED.,.F.,.F.)
B_SPLINE_CURVE_WITH_KNOTS((3,3),(0.14973948338295,0.97160236658079),
 .UNSPECIFIED.)
CURVE()
GEOMETRIC_REPRESENTATION_ITEM()
RATIONAL_B_SPLINE_CURVE((1.07140024848292,1.23714644374248,1.07140024848292))
REPRESENTATION_ITEM('')
);
#21=(
BOUNDED_CURVE()
B_SPLINE_CURVE(2,(#10960,#10961,#10962),.UNSPECIFIED.,.F.,.F.)
B_SPLINE_CURVE_WITH_KNOTS((3,3),(0.14973948338295,0.97160236658079),
 .UNSPECIFIED.)
CURVE()
GEOMETRIC_REPRESENTATION_ITEM()
RATIONAL_B_SPLINE_CURVE((1.07140024848292,1.23714644374248,1.07140024848292))
REPRESENTATION_ITEM('')
);
#22=(
BOUNDED_CURVE()
B_SPLINE_CURVE(2,(#10963,#10964,#10965),.UNSPECIFIED.,.F.,.F.)
B_SPLINE_CURVE_WITH_KNOTS((3,3),(0.14973948338295,0.971602366580789),
 .UNSPECIFIED.)
CURVE()
GEOMETRIC_REPRESENTATION_ITEM()
RATIONAL_B_SPLINE_CURVE((1.07140024848292,1.23714644374248,1.07140024848292))
REPRESENTATION_ITEM('')
);
#403=CONICAL_SURFACE('',#7143,0.734027674973257,1.0471975511966);
#404=CONICAL_SURFACE('',#7145,0.734027674973257,1.0471975511966);
#438=SHAPE_REPRESENTATION_RELATIONSHIP('SRR','None',#11747,#470);
#470=ADVANCED_BREP_SHAPE_REPRESENTATION('',(#533),#11549);
#503=STYLED_ITEM('',(#11974),#533);
#533=MANIFOLD_SOLID_BREP('Body1',#6351);
#651=FACE_BOUND('',#1635,.T.);
#652=FACE_BOUND('',#1637,.T.);
#852=PLANE('',#7147);
#853=PLANE('',#7148);
#854=PLANE('',#7149);
#855=PLANE('',#7153);
#856=PLANE('',#7154);
#857=PLANE('',#7155);
#858=PLANE('',#7156);
#859=PLANE('',#7157);
#1172=FACE_OUTER_BOUND('',#1625,.T.);
#1173=FACE_OUTER_BOUND('',#1626,.T.);
#1174=FACE_OUTER_BOUND('',#1627,.T.);
#1175=FACE_OUTER_BOUND('',#1628,.T.);
#1176=FACE_OUTER_BOUND('',#1629,.T.);
#1177=FACE_OUTER_BOUND('',#1630,.T.);
#1178=FACE_OUTER_BOUND('',#1631,.T.);
#1179=FACE_OUTER_BOUND('',#1632,.T.);
#1180=FACE_OUTER_BOUND('',#1633,.T.);
#1181=FACE_OUTER_BOUND('',#1634,.T.);
#1182=FACE_OUTER_BOUND('',#1636,.T.);
#1625=EDGE_LOOP('',(#5506,#5507,#5508,#5509,#5510,#5511,#5512,#5513,#5514));
#1626=EDGE_LOOP('',(#5515,#5516,#5517,#5518,#5519,#5520,#5521,#5522,#5523));
#1627=EDGE_LOOP('',(#5524,#5525,#5526,#5527));
#1628=EDGE_LOOP('',(#5528,#5529,#5530,#5531));
#1629=EDGE_LOOP('',(#5532,#5533,#5534,#5535));
#1630=EDGE_LOOP('',(#5536,#5537,#5538,#5539));
#1631=EDGE_LOOP('',(#5540,#5541,#5542,#5543));
#1632=EDGE_LOOP('',(#5544,#5545,#5546,#5547));
#1633=EDGE_LOOP('',(#5548,#5549,#5550,#5551));
#1634=EDGE_LOOP('',(#5552));
#1635=EDGE_LOOP('',(#5553));
#1636=EDGE_LOOP('',(#5554));
#1637=EDGE_LOOP('',(#5555));
#2160=LINE('',#10921,#2707);
#2161=LINE('',#10942,#2708);
#2162=LINE('',#10967,#2709);
#2163=LINE('',#10968,#2710);
#2164=LINE('',#10970,#2711);
#2165=LINE('',#10972,#2712);
#2166=LINE('',#10977,#2713);
#2167=LINE('',#10980,#2714);
#2168=LINE('',#10982,#2715);
#2707=VECTOR('',#8651,0.734027674973257);
#2708=VECTOR('',#8658,0.734027674973257);
#2709=VECTOR('',#8661,1.);
#2710=VECTOR('',#8662,1.);
#2711=VECTOR('',#8665,1.);
#2712=VECTOR('',#8668,1.);
#2713=VECTOR('',#8673,0.4);
#2714=VECTOR('',#8678,1.);
#2715=VECTOR('',#8681,1.);
#2980=CIRCLE('',#7144,0.6175);
#2981=CIRCLE('',#7146,0.6175);
#2982=CIRCLE('',#7151,0.338975);
#2983=CIRCLE('',#7152,0.338975);
#3423=VERTEX_POINT('',#10911);
#3424=VERTEX_POINT('',#10912);
#3425=VERTEX_POINT('',#10916);
#3426=VERTEX_POINT('',#10920);
#3427=VERTEX_POINT('',#10923);
#3428=VERTEX_POINT('',#10927);
#3429=VERTEX_POINT('',#10931);
#3430=VERTEX_POINT('',#10939);
#3431=VERTEX_POINT('',#10941);
#3432=VERTEX_POINT('',#10943);
#3433=VERTEX_POINT('',#10947);
#3434=VERTEX_POINT('',#10951);
#3435=VERTEX_POINT('',#10955);
#3436=VERTEX_POINT('',#10959);
#3437=VERTEX_POINT('',#10974);
#3438=VERTEX_POINT('',#10976);
#4138=EDGE_CURVE('',#3423,#3424,#11,.T.);
#4139=EDGE_CURVE('',#3425,#3423,#12,.T.);
#4140=EDGE_CURVE('',#3425,#3426,#2160,.T.);
#4141=EDGE_CURVE('',#3426,#3426,#2980,.T.);
#4142=EDGE_CURVE('',#3427,#3425,#13,.T.);
#4143=EDGE_CURVE('',#3428,#3427,#14,.T.);
#4144=EDGE_CURVE('',#3429,#3428,#15,.T.);
#4145=EDGE_CURVE('',#3424,#3429,#16,.T.);
#4146=EDGE_CURVE('',#3430,#3430,#2981,.T.);
#4147=EDGE_CURVE('',#3430,#3431,#2161,.T.);
#4148=EDGE_CURVE('',#3432,#3431,#17,.T.);
#4149=EDGE_CURVE('',#3433,#3432,#18,.T.);
#4150=EDGE_CURVE('',#3434,#3433,#19,.T.);
#4151=EDGE_CURVE('',#3435,#3434,#20,.T.);
#4152=EDGE_CURVE('',#3436,#3435,#21,.T.);
#4153=EDGE_CURVE('',#3431,#3436,#22,.T.);
#4154=EDGE_CURVE('',#3427,#3436,#2162,.T.);
#4155=EDGE_CURVE('',#3428,#3435,#2163,.T.);
#4156=EDGE_CURVE('',#3425,#3431,#2164,.T.);
#4157=EDGE_CURVE('',#3423,#3432,#2165,.T.);
#4158=EDGE_CURVE('',#3437,#3437,#2982,.F.);
#4159=EDGE_CURVE('',#3437,#3438,#2166,.T.);
#4160=EDGE_CURVE('',#3438,#3438,#2983,.F.);
#4161=EDGE_CURVE('',#3424,#3433,#2167,.T.);
#4162=EDGE_CURVE('',#3429,#3434,#2168,.T.);
#5506=ORIENTED_EDGE('',*,*,#4138,.F.);
#5507=ORIENTED_EDGE('',*,*,#4139,.F.);
#5508=ORIENTED_EDGE('',*,*,#4140,.T.);
#5509=ORIENTED_EDGE('',*,*,#4141,.F.);
#5510=ORIENTED_EDGE('',*,*,#4140,.F.);
#5511=ORIENTED_EDGE('',*,*,#4142,.F.);
#5512=ORIENTED_EDGE('',*,*,#4143,.F.);
#5513=ORIENTED_EDGE('',*,*,#4144,.F.);
#5514=ORIENTED_EDGE('',*,*,#4145,.F.);
#5515=ORIENTED_EDGE('',*,*,#4146,.F.);
#5516=ORIENTED_EDGE('',*,*,#4147,.T.);
#5517=ORIENTED_EDGE('',*,*,#4148,.F.);
#5518=ORIENTED_EDGE('',*,*,#4149,.F.);
#5519=ORIENTED_EDGE('',*,*,#4150,.F.);
#5520=ORIENTED_EDGE('',*,*,#4151,.F.);
#5521=ORIENTED_EDGE('',*,*,#4152,.F.);
#5522=ORIENTED_EDGE('',*,*,#4153,.F.);
#5523=ORIENTED_EDGE('',*,*,#4147,.F.);
#5524=ORIENTED_EDGE('',*,*,#4143,.T.);
#5525=ORIENTED_EDGE('',*,*,#4154,.T.);
#5526=ORIENTED_EDGE('',*,*,#4152,.T.);
#5527=ORIENTED_EDGE('',*,*,#4155,.F.);
#5528=ORIENTED_EDGE('',*,*,#4142,.T.);
#5529=ORIENTED_EDGE('',*,*,#4156,.T.);
#5530=ORIENTED_EDGE('',*,*,#4153,.T.);
#5531=ORIENTED_EDGE('',*,*,#4154,.F.);
#5532=ORIENTED_EDGE('',*,*,#4139,.T.);
#5533=ORIENTED_EDGE('',*,*,#4157,.T.);
#5534=ORIENTED_EDGE('',*,*,#4148,.T.);
#5535=ORIENTED_EDGE('',*,*,#4156,.F.);
#5536=ORIENTED_EDGE('',*,*,#4158,.F.);
#5537=ORIENTED_EDGE('',*,*,#4159,.T.);
#5538=ORIENTED_EDGE('',*,*,#4160,.T.);
#5539=ORIENTED_EDGE('',*,*,#4159,.F.);
#5540=ORIENTED_EDGE('',*,*,#4138,.T.);
#5541=ORIENTED_EDGE('',*,*,#4161,.T.);
#5542=ORIENTED_EDGE('',*,*,#4149,.T.);
#5543=ORIENTED_EDGE('',*,*,#4157,.F.);
#5544=ORIENTED_EDGE('',*,*,#4144,.T.);
#5545=ORIENTED_EDGE('',*,*,#4155,.T.);
#5546=ORIENTED_EDGE('',*,*,#4151,.T.);
#5547=ORIENTED_EDGE('',*,*,#4162,.F.);
#5548=ORIENTED_EDGE('',*,*,#4145,.T.);
#5549=ORIENTED_EDGE('',*,*,#4162,.T.);
#5550=ORIENTED_EDGE('',*,*,#4150,.T.);
#5551=ORIENTED_EDGE('',*,*,#4161,.F.);
#5552=ORIENTED_EDGE('',*,*,#4146,.T.);
#5553=ORIENTED_EDGE('',*,*,#4158,.T.);
#5554=ORIENTED_EDGE('',*,*,#4141,.T.);
#5555=ORIENTED_EDGE('',*,*,#4160,.F.);
#5960=CYLINDRICAL_SURFACE('',#7150,0.338975);
#6235=ADVANCED_FACE('',(#1172),#403,.T.);
#6236=ADVANCED_FACE('',(#1173),#404,.T.);
#6237=ADVANCED_FACE('',(#1174),#852,.T.);
#6238=ADVANCED_FACE('',(#1175),#853,.T.);
#6239=ADVANCED_FACE('',(#1176),#854,.T.);
#6240=ADVANCED_FACE('',(#1177),#5960,.F.);
#6241=ADVANCED_FACE('',(#1178),#855,.T.);
#6242=ADVANCED_FACE('',(#1179),#856,.T.);
#6243=ADVANCED_FACE('',(#1180),#857,.T.);
#6244=ADVANCED_FACE('',(#1181,#651),#858,.T.);
#6245=ADVANCED_FACE('',(#1182,#652),#859,.F.);
#6351=CLOSED_SHELL('',(#6235,#6236,#6237,#6238,#6239,#6240,#6241,#6242,
#6243,#6244,#6245));
#7142=AXIS2_PLACEMENT_3D('',#10909,#8647,#8648);
#7143=AXIS2_PLACEMENT_3D('',#10910,#8649,#8650);
#7144=AXIS2_PLACEMENT_3D('',#10922,#8652,#8653);
#7145=AXIS2_PLACEMENT_3D('',#10938,#8654,#8655);
#7146=AXIS2_PLACEMENT_3D('',#10940,#8656,#8657);
#7147=AXIS2_PLACEMENT_3D('',#10966,#8659,#8660);
#7148=AXIS2_PLACEMENT_3D('',#10969,#8663,#8664);
#7149=AXIS2_PLACEMENT_3D('',#10971,#8666,#8667);
#7150=AXIS2_PLACEMENT_3D('',#10973,#8669,#8670);
#7151=AXIS2_PLACEMENT_3D('',#10975,#8671,#8672);
#7152=AXIS2_PLACEMENT_3D('',#10978,#8674,#8675);
#7153=AXIS2_PLACEMENT_3D('',#10979,#8676,#8677);
#7154=AXIS2_PLACEMENT_3D('',#10981,#8679,#8680);
#7155=AXIS2_PLACEMENT_3D('',#10983,#8682,#8683);
#7156=AXIS2_PLACEMENT_3D('',#10984,#8684,#8685);
#7157=AXIS2_PLACEMENT_3D('',#10985,#8686,#8687);
#8647=DIRECTION('axis',(0.,0.,1.));
#8648=DIRECTION('refdir',(1.,0.,0.));
#8649=DIRECTION('center_axis',(0.,1.,0.));
#8650=DIRECTION('ref_axis',(1.,0.,0.));
#8651=DIRECTION('',(0.866025403784439,-0.5,1.06057523872491E-16));
#8652=DIRECTION('center_axis',(0.,-1.,0.));
#8653=DIRECTION('ref_axis',(1.,0.,0.));
#8654=DIRECTION('center_axis',(0.,-1.,0.));
#8655=DIRECTION('ref_axis',(1.,0.,0.));
#8656=DIRECTION('center_axis',(0.,1.,0.));
#8657=DIRECTION('ref_axis',(1.,0.,0.));
#8658=DIRECTION('',(-0.866025403784439,-0.5,-1.06057523872491E-16));
#8659=DIRECTION('center_axis',(1.4792020664489E-16,0.,-1.));
#8660=DIRECTION('ref_axis',(-1.,0.,-1.4792020664489E-16));
#8661=DIRECTION('',(0.,1.,0.));
#8662=DIRECTION('',(0.,1.,0.));
#8663=DIRECTION('center_axis',(-0.866025403784439,0.,-0.5));
#8664=DIRECTION('ref_axis',(-0.5,0.,0.866025403784439));
#8665=DIRECTION('',(0.,1.,0.));
#8666=DIRECTION('center_axis',(-0.866025403784439,0.,0.5));
#8667=DIRECTION('ref_axis',(0.5,0.,0.866025403784439));
#8668=DIRECTION('',(0.,1.,0.));
#8669=DIRECTION('center_axis',(0.,1.,0.));
#8670=DIRECTION('ref_axis',(1.,0.,0.));
#8671=DIRECTION('center_axis',(0.,1.,0.));
#8672=DIRECTION('ref_axis',(1.,0.,0.));
#8673=DIRECTION('',(0.,-1.,0.));
#8674=DIRECTION('center_axis',(0.,1.,0.));
#8675=DIRECTION('ref_axis',(1.,0.,0.));
#8676=DIRECTION('center_axis',(-2.95840413289779E-16,0.,1.));
#8677=DIRECTION('ref_axis',(1.,0.,2.95840413289779E-16));
#8678=DIRECTION('',(0.,1.,0.));
#8679=DIRECTION('center_axis',(0.866025403784439,0.,-0.5));
#8680=DIRECTION('ref_axis',(-0.5,0.,-0.866025403784439));
#8681=DIRECTION('',(0.,1.,0.));
#8682=DIRECTION('center_axis',(0.866025403784439,0.,0.5));
#8683=DIRECTION('ref_axis',(0.5,0.,-0.866025403784439));
#8684=DIRECTION('center_axis',(0.,1.,0.));
#8685=DIRECTION('ref_axis',(1.,0.,0.));
#8686=DIRECTION('center_axis',(0.,1.,0.));
#8687=DIRECTION('ref_axis',(1.,0.,0.));
#10909=CARTESIAN_POINT('',(0.,0.,0.));
#10910=CARTESIAN_POINT('Origin',(0.,0.067277284513851,0.));
#10911=CARTESIAN_POINT('',(-0.375277674973257,0.0768195421087395,0.65));
#10912=CARTESIAN_POINT('',(0.375277674973257,0.0768195421087395,0.65));
#10913=CARTESIAN_POINT('Ctrl Pts',(-0.375277674973257,0.0768195421087395,
0.65));
#10914=CARTESIAN_POINT('Ctrl Pts',(1.66533453693773E-13,-0.0315137912242439,
0.65));
#10915=CARTESIAN_POINT('Ctrl Pts',(0.375277674973257,0.0768195421087394,
0.65));
#10916=CARTESIAN_POINT('',(-0.750555349946514,0.0768195421087394,-9.19165206894919E-17));
#10917=CARTESIAN_POINT('Ctrl Pts',(-0.750555349946514,0.0768195421087394,
-9.19165206894919E-17));
#10918=CARTESIAN_POINT('Ctrl Pts',(-0.562916512459802,-0.0315137912242434,
0.325000000000144));
#10919=CARTESIAN_POINT('Ctrl Pts',(-0.375277674973257,0.0768195421087395,
0.65));
#10920=CARTESIAN_POINT('',(-0.6175,-2.77555756156289E-17,-7.5621939847349E-17));
#10921=CARTESIAN_POINT('',(-0.734027674973257,0.067277284513851,-8.98924642641573E-17));
#10922=CARTESIAN_POINT('Origin',(0.,0.,0.));
#10923=CARTESIAN_POINT('',(-0.375277674973257,0.0768195421087395,-0.65));
#10924=CARTESIAN_POINT('Ctrl Pts',(-0.375277674973257,0.0768195421087395,
-0.65));
#10925=CARTESIAN_POINT('Ctrl Pts',(-0.562916512459968,-0.0315137912242437,
-0.324999999999856));
#10926=CARTESIAN_POINT('Ctrl Pts',(-0.750555349946514,0.0768195421087395,
-9.19165206894919E-17));
#10927=CARTESIAN_POINT('',(0.375277674973257,0.0768195421087395,-0.65));
#10928=CARTESIAN_POINT('Ctrl Pts',(0.375277674973257,0.0768195421087395,
-0.65));
#10929=CARTESIAN_POINT('Ctrl Pts',(-1.66144875635155E-13,-0.0315137912242437,
-0.65));
#10930=CARTESIAN_POINT('Ctrl Pts',(-0.375277674973257,0.0768195421087395,
-0.65));
#10931=CARTESIAN_POINT('',(0.750555349946514,0.0768195421087394,0.));
#10932=CARTESIAN_POINT('Ctrl Pts',(0.750555349946514,0.0768195421087394,
0.));
#10933=CARTESIAN_POINT('Ctrl Pts',(0.562916512459802,-0.0315137912242436,
-0.325000000000144));
#10934=CARTESIAN_POINT('Ctrl Pts',(0.375277674973257,0.0768195421087395,
-0.65));
#10935=CARTESIAN_POINT('Ctrl Pts',(0.375277674973257,0.0768195421087394,
0.65));
#10936=CARTESIAN_POINT('Ctrl Pts',(0.562916512459968,-0.0315137912242439,
0.324999999999856));
#10937=CARTESIAN_POINT('Ctrl Pts',(0.750555349946514,0.0768195421087394,
0.));
#10938=CARTESIAN_POINT('Origin',(0.,0.612722715486149,0.));
#10939=CARTESIAN_POINT('',(-0.6175,0.68,-7.5621939847349E-17));
#10940=CARTESIAN_POINT('Origin',(0.,0.68,0.));
#10941=CARTESIAN_POINT('',(-0.750555349946514,0.603180457891261,-9.19165206894919E-17));
#10942=CARTESIAN_POINT('',(-0.734027674973257,0.612722715486149,-8.98924642641573E-17));
#10943=CARTESIAN_POINT('',(-0.375277674973257,0.603180457891261,0.65));
#10944=CARTESIAN_POINT('Ctrl Pts',(-0.375277674973257,0.603180457891261,
0.65));
#10945=CARTESIAN_POINT('Ctrl Pts',(-0.562916512459968,0.711513791224243,
0.324999999999856));
#10946=CARTESIAN_POINT('Ctrl Pts',(-0.750555349946514,0.603180457891261,
-9.19165206894919E-17));
#10947=CARTESIAN_POINT('',(0.375277674973257,0.603180457891261,0.65));
#10948=CARTESIAN_POINT('Ctrl Pts',(0.375277674973257,0.603180457891261,
0.65));
#10949=CARTESIAN_POINT('Ctrl Pts',(-1.66755498298699E-13,0.711513791224244,
0.65));
#10950=CARTESIAN_POINT('Ctrl Pts',(-0.375277674973257,0.603180457891261,
0.65));
#10951=CARTESIAN_POINT('',(0.750555349946514,0.603180457891261,0.));
#10952=CARTESIAN_POINT('Ctrl Pts',(0.750555349946514,0.603180457891261,
0.));
#10953=CARTESIAN_POINT('Ctrl Pts',(0.562916512459802,0.711513791224244,
0.325000000000144));
#10954=CARTESIAN_POINT('Ctrl Pts',(0.375277674973257,0.603180457891261,
0.65));
#10955=CARTESIAN_POINT('',(0.375277674973257,0.603180457891261,-0.65));
#10956=CARTESIAN_POINT('Ctrl Pts',(0.375277674973257,0.603180457891261,
-0.65));
#10957=CARTESIAN_POINT('Ctrl Pts',(0.562916512459969,0.711513791224244,
-0.324999999999856));
#10958=CARTESIAN_POINT('Ctrl Pts',(0.750555349946514,0.603180457891261,
0.));
#10959=CARTESIAN_POINT('',(-0.375277674973257,0.603180457891261,-0.65));
#10960=CARTESIAN_POINT('Ctrl Pts',(-0.375277674973257,0.603180457891261,
-0.65));
#10961=CARTESIAN_POINT('Ctrl Pts',(1.66422431391311E-13,0.711513791224244,
-0.65));
#10962=CARTESIAN_POINT('Ctrl Pts',(0.375277674973257,0.603180457891261,
-0.65));
#10963=CARTESIAN_POINT('Ctrl Pts',(-0.750555349946514,0.603180457891261,
-9.19165206894919E-17));
#10964=CARTESIAN_POINT('Ctrl Pts',(-0.562916512459802,0.711513791224244,
-0.325000000000144));
#10965=CARTESIAN_POINT('Ctrl Pts',(-0.375277674973257,0.603180457891261,
-0.65));
#10966=CARTESIAN_POINT('Origin',(0.375277674973257,0.,-0.65));
#10967=CARTESIAN_POINT('',(-0.375277674973257,0.,-0.65));
#10968=CARTESIAN_POINT('',(0.375277674973257,0.,-0.65));
#10969=CARTESIAN_POINT('Origin',(-0.375277674973257,0.,-0.65));
#10970=CARTESIAN_POINT('',(-0.750555349946514,0.,-9.19165206894919E-17));
#10971=CARTESIAN_POINT('Origin',(-0.750555349946514,0.,-9.19165206894919E-17));
#10972=CARTESIAN_POINT('',(-0.375277674973257,0.,0.65));
#10973=CARTESIAN_POINT('Origin',(0.,0.,0.));
#10974=CARTESIAN_POINT('',(-0.338975,0.68,4.15124648740974E-17));
#10975=CARTESIAN_POINT('Origin',(0.,0.68,0.));
#10976=CARTESIAN_POINT('',(-0.338975,0.,4.15124648740974E-17));
#10977=CARTESIAN_POINT('',(-0.338975,0.,4.15124648740974E-17));
#10978=CARTESIAN_POINT('Origin',(0.,0.,0.));
#10979=CARTESIAN_POINT('Origin',(-0.375277674973257,0.,0.65));
#10980=CARTESIAN_POINT('',(0.375277674973257,0.,0.65));
#10981=CARTESIAN_POINT('Origin',(0.750555349946514,0.,0.));
#10982=CARTESIAN_POINT('',(0.750555349946514,0.,0.));
#10983=CARTESIAN_POINT('Origin',(0.375277674973257,0.,0.65));
#10984=CARTESIAN_POINT('Origin',(0.,0.68,-1.11022302462516E-16));
#10985=CARTESIAN_POINT('Origin',(0.,0.,-1.11022302462516E-16));
#11512=UNCERTAINTY_MEASURE_WITH_UNIT(LENGTH_MEASURE(0.001),#11560,
'DISTANCE_ACCURACY_VALUE',
'Maximum model space distance between geometric entities at asserted c
onnectivities');
#11522=UNCERTAINTY_MEASURE_WITH_UNIT(LENGTH_MEASURE(0.001),#11560,
'DISTANCE_ACCURACY_VALUE',
'Maximum model space distance between geometric entities at asserted c
onnectivities');
#11549=(
GEOMETRIC_REPRESENTATION_CONTEXT(3)
GLOBAL_UNCERTAINTY_ASSIGNED_CONTEXT((#11512))
GLOBAL_UNIT_ASSIGNED_CONTEXT((#11560,#11562,#11563))
REPRESENTATION_CONTEXT('','3D')
);
#11559=(
GEOMETRIC_REPRESENTATION_CONTEXT(3)
GLOBAL_UNCERTAINTY_ASSIGNED_CONTEXT((#11522))
GLOBAL_UNIT_ASSIGNED_CONTEXT((#11560,#11562,#11563))
REPRESENTATION_CONTEXT('','3D')
);
#11560=(
LENGTH_UNIT()
NAMED_UNIT(*)
SI_UNIT(.CENTI.,.METRE.)
);
#11562=(
NAMED_UNIT(*)
PLANE_ANGLE_UNIT()
SI_UNIT($,.RADIAN.)
);
#11563=(
NAMED_UNIT(*)
SI_UNIT($,.STERADIAN.)
SOLID_ANGLE_UNIT()
);
#11590=SHAPE_DEFINITION_REPRESENTATION(#11628,#11747);
#11628=PRODUCT_DEFINITION_SHAPE('',$,#11784);
#11747=SHAPE_REPRESENTATION('',(#7142),#11549);
#11757=PRODUCT_DEFINITION_CONTEXT('part definition',#11867,'design');
#11784=PRODUCT_DEFINITION('Hex Nut - M8','Hex Nut - M8',#11820,#11757);
#11820=PRODUCT_DEFINITION_FORMATION('',$,#11895);
#11867=APPLICATION_CONTEXT(
'Core Data for Automotive Mechanical Design Process');
#11868=PRODUCT_CONTEXT('part definition',#11867,'mechanical');
#11895=PRODUCT('Hex Nut - M8','Hex Nut - M8','Hex Nut - M8',(#11868));
#11968=COLOUR_RGB('Black',0.12,0.14,0.17);
#11969=FILL_AREA_STYLE_COLOUR('',#11968);
#11970=FILL_AREA_STYLE('',(#11969));
#11971=SURFACE_STYLE_FILL_AREA(#11970);
#11972=SURFACE_SIDE_STYLE('',(#11971));
#11973=SURFACE_STYLE_USAGE(.BOTH.,#11972);
#11974=PRESENTATION_STYLE_ASSIGNMENT((#11973));
ENDSEC;
END-ISO-10303-21;
